ISO-10303-21;
HEADER;
FILE_DESCRIPTION (('STEP AP203'),
    '1' );
FILE_NAME ('F3.step',
    '2026-10-31T14:11:27',
    ( '' ),
    ( '' ),
    'SwSTEP 2.0',
    'SolidWorks 2024',
    '' );
FILE_SCHEMA (( 'AUTOMOTIVE_DESIGN' ));
ENDSEC;

DATA;
#32=EDGE_CURVE ( 'NONE', #6326, #3176, #10614, .T. ) ;
#75=AXIS2_PLACEMENT_3D ( 'NONE', #11008, #20130, #11135 ) ;
#89=ORIENTED_EDGE ( 'NONE', *, *, #15771, .F. ) ;
#93=VECTOR ( 'NONE', #17337, 1000.000000000000000 ) ;
#121=LINE ( 'NONE', #10734, #5080 ) ;
#138=CIRCLE ( 'NONE', #3191, 2.500000000000000000 ) ;
#149=CARTESIAN_POINT ( 'NONE',  ( -27.00000000000000000, -27.34999999999999787, 6.250000000000000000 ) ) ;
#163=DESIGN_CONTEXT ( 'detailed design', #14471, 'design' ) ;
#172=DIRECTION ( 'NONE',  ( -2.977235988022386522E-185, 9.605990953944227443E-124, 1.000000000000000000 ) ) ;
#188=LINE ( 'NONE', #7456, #8973 ) ;
#218=CARTESIAN_POINT ( 'NONE',  ( 2.500000000000026645, -7.535786464196452844E-15, 2.500000000000000000 ) ) ;
#223=EDGE_LOOP ( 'NONE', ( #4178, #13372, #15344, #5605 ) ) ;
#274=AXIS2_PLACEMENT_3D ( 'NONE', #4607, #15649, #6504 ) ;
#289=EDGE_CURVE ( 'NONE', #8641, #12606, #10851, .T. ) ;
#384=ADVANCED_FACE ( 'NONE', ( #22889, #4726, #13202, #10087 ), #14970, .T. ) ;
#395=CYLINDRICAL_SURFACE ( 'NONE', #18197, 2.500000000000000888 ) ;
#415=DIRECTION ( 'NONE',  ( 1.000000000000000000, 0.000000000000000000, 0.000000000000000000 ) ) ;
#512=CARTESIAN_POINT ( 'NONE',  ( 2.664535259100379799E-14, -1.554450629062440126E-15, 2.500000000000000000 ) ) ;
#530=EDGE_CURVE ( 'NONE', #16237, #5287, #3326, .T. ) ;
#555=EDGE_CURVE ( 'NONE', #17008, #6563, #19274, .T. ) ;
#625=ADVANCED_FACE ( 'NONE', ( #1615 ), #14571, .T. ) ;
#687=VERTEX_POINT ( 'NONE', #5647 ) ;
#751=VECTOR ( 'NONE', #11337, 1000.000000000000000 ) ;
#810=FACE_OUTER_BOUND ( 'NONE', #9895, .T. ) ;
#837=AXIS2_PLACEMENT_3D ( 'NONE', #5349, #16154, #3336 ) ;
#896=VECTOR ( 'NONE', #18174, 1000.000000000000000 ) ;
#898=FACE_OUTER_BOUND ( 'NONE', #11137, .T. ) ;
#933=DIRECTION ( 'NONE',  ( 0.7071067811865476838, -1.387778780781444689E-15, 0.7071067811865473507 ) ) ;
#988=DIRECTION ( 'NONE',  ( -3.099353312215988811E-62, -9.818186930595456717E-93, 1.000000000000000000 ) ) ;
#994=ORIENTED_EDGE ( 'NONE', *, *, #10741, .F. ) ;
#1003=DIRECTION ( 'NONE',  ( -3.099353312215988811E-62, 2.485476484129594803E-78, 1.000000000000000000 ) ) ;
#1021=ORIENTED_EDGE ( 'NONE', *, *, #17513, .F. ) ;
#1067=EDGE_CURVE ( 'NONE', #11527, #12850, #6836, .T. ) ;
#1085=CLOSED_SHELL ( 'NONE', ( #12715, #9280, #8950, #16235, #5596, #17857, #8299, #2010, #10563, #625, #19739, #11686, #14339, #12107, #384, #18950, #16345, #13405, #7191, #12169, #14207, #10751, #7480, #19339, #20276 ) ) ;
#1121=DIRECTION ( 'NONE',  ( -3.099353312215989243E-62, 2.537976065170614732E-77, 1.000000000000000000 ) ) ;
#1125=ORIENTED_EDGE ( 'NONE', *, *, #8683, .F. ) ;
#1191=FACE_OUTER_BOUND ( 'NONE', #3998, .T. ) ;
#1194=VECTOR ( 'NONE', #12004, 1000.000000000000000 ) ;
#1252=EDGE_CURVE ( 'NONE', #11510, #1465, #20380, .T. ) ;
#1291=DIRECTION ( 'NONE',  ( -2.270069654138865127E-15, -1.000000000000000000, -4.574083617919690056E-30 ) ) ;
#1296=VERTEX_POINT ( 'NONE', #21999 ) ;
#1302=DIRECTION ( 'NONE',  ( -2.977235988022386522E-185, 9.605990953944227443E-124, 1.000000000000000000 ) ) ;
#1339=UNCERTAINTY_MEASURE_WITH_UNIT (LENGTH_MEASURE( 1.000000000000000082E-05 ), #22266, 'distance_accuracy_value', 'NONE');
#1351=CARTESIAN_POINT ( 'NONE',  ( -4.514225866272930432, 4.676725866273569565, 5.000000000000000000 ) ) ;
#1417=AXIS2_PLACEMENT_3D ( 'NONE', #4886, #13553, #4526 ) ;
#1446=ORIENTED_EDGE ( 'NONE', *, *, #19798, .F. ) ;
#1465=VERTEX_POINT ( 'NONE', #6226 ) ;
#1550=LINE ( 'NONE', #21502, #5395 ) ;
#1566=DIRECTION ( 'NONE',  ( -1.000000000000000000, 2.270069654138870255E-15, -3.099353312215989243E-62 ) ) ;
#1615=FACE_OUTER_BOUND ( 'NONE', #12145, .T. ) ;
#1622=AXIS2_PLACEMENT_3D ( 'NONE', #11661, #22434, #16729 ) ;
#1626=ORIENTED_EDGE ( 'NONE', *, *, #11578, .T. ) ;
#1665=ORIENTED_EDGE ( 'NONE', *, *, #19845, .T. ) ;
#1666=ORIENTED_EDGE ( 'NONE', *, *, #16477, .F. ) ;
#1674=CARTESIAN_POINT ( 'NONE',  ( -27.00000000000000000, -30.47499999999999787, 19.00000000000000000 ) ) ;
#1786=CARTESIAN_POINT ( 'NONE',  ( -27.00000000000000000, -28.60000000000000142, 21.50000000000000000 ) ) ;
#1833=DIRECTION ( 'NONE',  ( -3.099353312215989243E-62, -1.872670541876879671E-92, 1.000000000000000000 ) ) ;
#1839=ORIENTED_EDGE ( 'NONE', *, *, #15220, .T. ) ;
#1856=CYLINDRICAL_SURFACE ( 'NONE', #21887, 2.500000000000000000 ) ;
#1890=CARTESIAN_POINT ( 'NONE',  ( 5.000000000000000000, -28.60000000000000142, 6.250000000000000000 ) ) ;
#1900=ORIENTED_EDGE ( 'NONE', *, *, #20362, .F. ) ;
#1912=DIRECTION ( 'NONE',  ( -3.099353312215988811E-62, 1.001855809244433740E-92, 1.000000000000000000 ) ) ;
#1930=VECTOR ( 'NONE', #23331, 1000.000000000000000 ) ;
#1943=CYLINDRICAL_SURFACE ( 'NONE', #8490, 6.499999999999998224 ) ;
#1954=LINE ( 'NONE', #12886, #4264 ) ;
#1960=ORIENTED_EDGE ( 'NONE', *, *, #6381, .T. ) ;
#1964=ORIENTED_EDGE ( 'NONE', *, *, #8474, .F. ) ;
#1972=AXIS2_PLACEMENT_3D ( 'NONE', #15325, #13438, #2385 ) ;
#2010=ADVANCED_FACE ( 'NONE', ( #3087 ), #23028, .T. ) ;
#2027=CARTESIAN_POINT ( 'NONE',  ( 6.500000000000000000, -17.30000000000000071, 2.500000000000000000 ) ) ;
#2052=ORIENTED_EDGE ( 'NONE', *, *, #9969, .T. ) ;
#2076=ORIENTED_EDGE ( 'NONE', *, *, #20373, .F. ) ;
#2081=VERTEX_POINT ( 'NONE', #17594 ) ;
#2169=DIRECTION ( 'NONE',  ( 0.8846153846153629319, -0.4663213712685850276, 0.000000000000000000 ) ) ;
#2199=LINE ( 'NONE', #5532, #9602 ) ;
#2206=AXIS2_PLACEMENT_3D ( 'NONE', #15624, #8522, #1003 ) ;
#2208=LINE ( 'NONE', #18494, #20789 ) ;
#2300=EDGE_CURVE ( 'NONE', #16709, #6326, #16594, .T. ) ;
#2341=DIRECTION ( 'NONE',  ( -3.099353312215988811E-62, 0.000000000000000000, 1.000000000000000000 ) ) ;
#2371=DIRECTION ( 'NONE',  ( 0.000000000000000000, 3.098432463554639601E-31, 1.000000000000000000 ) ) ;
#2385=DIRECTION ( 'NONE',  ( 0.8846153846153629319, -0.4663213712685850276, 0.000000000000000000 ) ) ;
#2416=AXIS2_PLACEMENT_3D ( 'NONE', #16687, #6014, #20384 ) ;
#2438=AXIS2_PLACEMENT_3D ( 'NONE', #18783, #1291, #17921 ) ;
#2462=ORIENTED_EDGE ( 'NONE', *, *, #10309, .F. ) ;
#2569=CARTESIAN_POINT ( 'NONE',  ( 0.000000000000000000, 0.000000000000000000, 0.000000000000000000 ) ) ;
#2688=DIRECTION ( 'NONE',  ( -3.099353312215989243E-62, -9.818186930595456717E-93, 1.000000000000000000 ) ) ;
#2722=ORIENTED_EDGE ( 'NONE', *, *, #23317, .F. ) ;
#2761=EDGE_LOOP ( 'NONE', ( #17454, #2076, #20103, #12754 ) ) ;
#2784=DIRECTION ( 'NONE',  ( -3.099353312215989243E-62, -9.818186930595456717E-93, 1.000000000000000000 ) ) ;
#2800=LINE ( 'NONE', #16922, #6560 ) ;
#2837=ORIENTED_EDGE ( 'NONE', *, *, #20360, .F. ) ;
#2859=EDGE_LOOP ( 'NONE', ( #20950, #2722, #2052, #1964 ) ) ;
#2870=ORIENTED_EDGE ( 'NONE', *, *, #6668, .F. ) ;
#2875=CYLINDRICAL_SURFACE ( 'NONE', #10354, 2.500000000000000888 ) ;
#2891=VECTOR ( 'NONE', #19827, 1000.000000000000000 ) ;
#2896=DIRECTION ( 'NONE',  ( 1.000000000000000000, -2.611676738638919574E-15, 0.000000000000000000 ) ) ;
#2899=CARTESIAN_POINT ( 'NONE',  ( 4.267766952966340455, -30.47500000000000142, 20.76776695296636888 ) ) ;
#2906=CARTESIAN_POINT ( 'NONE',  ( -24.86147400983239919, -14.96352599016710094, 2.500000000000000000 ) ) ;
#2909=CARTESIAN_POINT ( 'NONE',  ( 5.000000000000000000, -31.09999999999999787, 19.00000000000000000 ) ) ;
#2924=VERTEX_POINT ( 'NONE', #12640 ) ;
#2983=CARTESIAN_POINT ( 'NONE',  ( -23.50000000000000000, -19.99999999999999289, 5.000000000000000000 ) ) ;
#3002=CARTESIAN_POINT ( 'NONE',  ( 2.499999999999970246, -28.60000000000000142, 21.50000000000000000 ) ) ;
#3036=EDGE_LOOP ( 'NONE', ( #22668, #10904, #8497, #7070 ) ) ;
#3044=EDGE_LOOP ( 'NONE', ( #13952, #10936, #14151, #1665 ) ) ;
#3087=FACE_OUTER_BOUND ( 'NONE', #3044, .T. ) ;
#3091=DIRECTION ( 'NONE',  ( -3.099353312215988811E-62, -9.818186930595456717E-93, 1.000000000000000000 ) ) ;
#3153=SHAPE_DEFINITION_REPRESENTATION ( #13679, #17646 ) ;
#3175=CARTESIAN_POINT ( 'NONE',  ( 5.000000000000000000, -28.60000000000000142, 6.250000000000000000 ) ) ;
#3176=VERTEX_POINT ( 'NONE', #19338 ) ;
#3178=ORIENTED_EDGE ( 'NONE', *, *, #21632, .F. ) ;
#3191=AXIS2_PLACEMENT_3D ( 'NONE', #6484, #21084, #11977 ) ;
#3222=DIRECTION ( 'NONE',  ( -3.099353312215989243E-62, -9.818186930595456717E-93, 1.000000000000000000 ) ) ;
#3290=CARTESIAN_POINT ( 'NONE',  ( -20.00000000000000000, -20.00000000000000000, 5.000000000000000000 ) ) ;
#3313=ORIENTED_EDGE ( 'NONE', *, *, #1067, .T. ) ;
#3326=CIRCLE ( 'NONE', #5225, 3.499999999999999556 ) ;
#3336=DIRECTION ( 'NONE',  ( 0.8846153846154060085, -0.4663213712685030377, 0.000000000000000000 ) ) ;
#3405=CARTESIAN_POINT ( 'NONE',  ( 2.664535259100379799E-14, -1.554450629062440126E-15, 2.500000000000000000 ) ) ;
#3533=DIRECTION ( 'NONE',  ( -1.000000000000000000, 2.270069654138870255E-15, 0.000000000000000000 ) ) ;
#3541=EDGE_CURVE ( 'NONE', #6526, #8301, #12203, .T. ) ;
#3571=EDGE_CURVE ( 'NONE', #12545, #6522, #9959, .T. ) ;
#3630=ORIENTED_EDGE ( 'NONE', *, *, #6357, .T. ) ;
#3638=VERTEX_POINT ( 'NONE', #12214 ) ;
#3648=FACE_OUTER_BOUND ( 'NONE', #2859, .T. ) ;
#3677=CARTESIAN_POINT ( 'NONE',  ( -20.00000000000000000, -20.00000000000000000, 2.500000000000000000 ) ) ;
#3705=CARTESIAN_POINT ( 'NONE',  ( -11.00000000000000000, -27.34999999999999787, 6.250000000000000000 ) ) ;
#3741=VERTEX_POINT ( 'NONE', #5178 ) ;
#3748=EDGE_CURVE ( 'NONE', #8909, #2924, #18689, .T. ) ;
#3828=ORIENTED_EDGE ( 'NONE', *, *, #16655, .T. ) ;
#3854=EDGE_CURVE ( 'NONE', #3176, #20610, #1954, .T. ) ;
#3856=DIRECTION ( 'NONE',  ( -2.270069654138870255E-15, -1.000000000000000000, -7.035747901516317327E-77 ) ) ;
#3865=ORIENTED_EDGE ( 'NONE', *, *, #19009, .F. ) ;
#3866=VECTOR ( 'NONE', #15647, 1000.000000000000000 ) ;
#3915=EDGE_CURVE ( 'NONE', #15256, #20661, #11095, .T. ) ;
#3923=PLANE ( 'NONE',  #12452 ) ;
#3978=ADVANCED_BREP_SHAPE_REPRESENTATION ( '', ( #17139, #12739 ), #19550 ) ;
#3998=EDGE_LOOP ( 'NONE', ( #22727, #15161, #8226, #7577 ) ) ;
#4043=ORIENTED_EDGE ( 'NONE', *, *, #19061, .F. ) ;
#4055=LINE ( 'NONE', #6068, #5249 ) ;
#4059=CARTESIAN_POINT ( 'NONE',  ( -26.26776695296636888, -30.47499999999999432, 20.76776695296636888 ) ) ;
#4149=FACE_OUTER_BOUND ( 'NONE', #14057, .T. ) ;
#4159=ORIENTED_EDGE ( 'NONE', *, *, #6668, .T. ) ;
#4178=ORIENTED_EDGE ( 'NONE', *, *, #16477, .T. ) ;
#4198=DIRECTION ( 'NONE',  ( -1.000000000000000000, 2.775557561562891351E-15, 0.000000000000000000 ) ) ;
#4246=VERTEX_POINT ( 'NONE', #4692 ) ;
#4264=VECTOR ( 'NONE', #3856, 1000.000000000000000 ) ;
#4268=ORIENTED_EDGE ( 'NONE', *, *, #6357, .F. ) ;
#4291=EDGE_LOOP ( 'NONE', ( #13978, #8585 ) ) ;
#4301=EDGE_CURVE ( 'NONE', #6326, #15757, #19080, .T. ) ;
#4318=EDGE_CURVE ( 'NONE', #11510, #17116, #17281, .T. ) ;
#4351=CARTESIAN_POINT ( 'NONE',  ( 6.500000000000000000, -17.30000000000000071, 2.500000000000000000 ) ) ;
#4394=CARTESIAN_POINT ( 'NONE',  ( -27.00000000000000000, -27.34999999999999787, 5.000000000000000000 ) ) ;
#4425=ORIENTED_EDGE ( 'NONE', *, *, #11909, .T. ) ;
#4526=DIRECTION ( 'NONE',  ( 0.000000000000000000, 0.000000000000000000, -1.000000000000000000 ) ) ;
#4565=EDGE_LOOP ( 'NONE', ( #9397, #22070, #6321, #18081, #1021, #15861, #16933, #18625 ) ) ;
#4576=PRODUCT ( 'F3', 'F3', '', ( #11149 ) ) ;
#4588=ORIENTED_EDGE ( 'NONE', *, *, #19798, .T. ) ;
#4607=CARTESIAN_POINT ( 'NONE',  ( -8.080225385240009217, -15.72171916155420313, 5.000000000000000000 ) ) ;
#4692=CARTESIAN_POINT ( 'NONE',  ( 2.499999999999970246, -31.09999999999999787, 21.50000000000000000 ) ) ;
#4695=ORIENTED_EDGE ( 'NONE', *, *, #16882, .F. ) ;
#4726=FACE_BOUND ( 'NONE', #5698, .T. ) ;
#4737=CARTESIAN_POINT ( 'NONE',  ( -4.514225866272930432, 4.676725866273559795, 2.500000000000000000 ) ) ;
#4796=CARTESIAN_POINT ( 'NONE',  ( 6.500000000000000000, -1.630990338096509915E-14, 2.500000000000000000 ) ) ;
#4798=CARTESIAN_POINT ( 'NONE',  ( -4.514225866272930432, 4.676725866273559795, 2.500000000000000000 ) ) ;
#4803=FACE_OUTER_BOUND ( 'NONE', #16877, .T. ) ;
#4824=VERTEX_POINT ( 'NONE', #7386 ) ;
#4854=ORIENTED_EDGE ( 'NONE', *, *, #6545, .F. ) ;
#4874=EDGE_CURVE ( 'NONE', #1296, #12606, #12167, .T. ) ;
#4886=CARTESIAN_POINT ( 'NONE',  ( 5.000000000000000000, -27.34999999999999787, 6.250000000000000000 ) ) ;
#4896=CARTESIAN_POINT ( 'NONE',  ( -27.00000000000000000, -28.60000000000000142, 6.250000000000000000 ) ) ;
#4907=DIRECTION ( 'NONE',  ( -1.000000000000000000, 2.270069654138870255E-15, 0.000000000000000000 ) ) ;
#4916=DIRECTION ( 'NONE',  ( -3.099353312215989243E-62, 0.000000000000000000, 1.000000000000000000 ) ) ;
#4921=DIRECTION ( 'NONE',  ( -3.099353312215988811E-62, 0.000000000000000000, 1.000000000000000000 ) ) ;
#4977=ORIENTED_EDGE ( 'NONE', *, *, #3854, .F. ) ;
#5026=CIRCLE ( 'NONE', #9598, 2.500000000000001776 ) ;
#5080=VECTOR ( 'NONE', #3091, 1000.000000000000000 ) ;
#5088=DIRECTION ( 'NONE',  ( 0.000000000000000000, 3.261507856373309729E-31, 1.000000000000000000 ) ) ;
#5133=FACE_OUTER_BOUND ( 'NONE', #4565, .T. ) ;
#5178=CARTESIAN_POINT ( 'NONE',  ( -2.499999999999973799, 4.120723506284736299E-15, 5.000000000000000000 ) ) ;
#5225=AXIS2_PLACEMENT_3D ( 'NONE', #3290, #16230, #9102 ) ;
#5235=DIRECTION ( 'NONE',  ( 2.270069654138865127E-15, 1.000000000000000000, -4.574083617919690056E-30 ) ) ;
#5238=CARTESIAN_POINT ( 'NONE',  ( 2.499999999999970246, -28.60000000000000142, 19.00000000000000000 ) ) ;
#5244=DIRECTION ( 'NONE',  ( -3.099353312215988811E-62, 0.000000000000000000, 1.000000000000000000 ) ) ;
#5249=VECTOR ( 'NONE', #11332, 1000.000000000000000 ) ;
#5265=DIRECTION ( 'NONE',  ( -1.000000000000000000, 2.270069654138870255E-15, -3.099353312215989243E-62 ) ) ;
#5285=AXIS2_PLACEMENT_3D ( 'NONE', #149, #5265, #10764 ) ;
#5287=VERTEX_POINT ( 'NONE', #5417 ) ;
#5291=VERTEX_POINT ( 'NONE', #20021 ) ;
#5349=CARTESIAN_POINT ( 'NONE',  ( -1.262685242559879909E-14, -17.30000000000000071, 2.500000000000000000 ) ) ;
#5395=VECTOR ( 'NONE', #7700, 1000.000000000000000 ) ;
#5403=CYLINDRICAL_SURFACE ( 'NONE', #23285, 3.499999999999999556 ) ;
#5417=CARTESIAN_POINT ( 'NONE',  ( -16.50000000000000000, -20.00000000000000711, 5.000000000000000000 ) ) ;
#5421=FACE_BOUND ( 'NONE', #11269, .T. ) ;
#5477=ORIENTED_EDGE ( 'NONE', *, *, #530, .T. ) ;
#5495=DIRECTION ( 'NONE',  ( 0.000000000000000000, 0.000000000000000000, -1.000000000000000000 ) ) ;
#5523=FACE_OUTER_BOUND ( 'NONE', #12129, .T. ) ;
#5532=CARTESIAN_POINT ( 'NONE',  ( 2.499999999999970246, -30.47499999999999787, 21.50000000000000000 ) ) ;
#5557=ORIENTED_EDGE ( 'NONE', *, *, #17513, .T. ) ;
#5579=ORIENTED_EDGE ( 'NONE', *, *, #6381, .F. ) ;
#5596=ADVANCED_FACE ( 'NONE', ( #6352 ), #20834, .T. ) ;
#5605=ORIENTED_EDGE ( 'NONE', *, *, #20170, .T. ) ;
#5611=ORIENTED_EDGE ( 'NONE', *, *, #1067, .F. ) ;
#5631=DIRECTION ( 'NONE',  ( -1.000000000000000000, 1.982541115402065307E-15, 0.000000000000000000 ) ) ;
#5634=CARTESIAN_POINT ( 'NONE',  ( -23.50000000000000000, -19.99999999999999289, 2.500000000000000000 ) ) ;
#5647=CARTESIAN_POINT ( 'NONE',  ( -27.00000000000000000, -20.00000000000000000, 2.500000000000000000 ) ) ;
#5654=DIRECTION ( 'NONE',  ( -1.000000000000000000, 2.270069654138870255E-15, 0.000000000000000000 ) ) ;
#5697=ORIENTED_EDGE ( 'NONE', *, *, #9792, .T. ) ;
#5698=EDGE_LOOP ( 'NONE', ( #21989, #20663 ) ) ;
#5756=CARTESIAN_POINT ( 'NONE',  ( 5.000000000000000000, -30.47499999999999787, 19.00000000000000000 ) ) ;
#5764=ORIENTED_EDGE ( 'NONE', *, *, #17683, .F. ) ;
#5766=FACE_BOUND ( 'NONE', #20069, .T. ) ;
#5812=AXIS2_PLACEMENT_3D ( 'NONE', #13567, #5860, #11230 ) ;
#5860=DIRECTION ( 'NONE',  ( 3.099353312215989243E-62, -2.689336210007789456E-77, -1.000000000000000000 ) ) ;
#5866=DIRECTION ( 'NONE',  ( -3.099353312215989243E-62, -1.872670541876879671E-92, 1.000000000000000000 ) ) ;
#5914=CARTESIAN_POINT ( 'NONE',  ( -27.00000000000000000, -28.60000000000000142, 21.50000000000000000 ) ) ;
#5942=CARTESIAN_POINT ( 'NONE',  ( -24.50000000000000000, -31.09999999999999787, 19.00000000000000000 ) ) ;
#5951=EDGE_CURVE ( 'NONE', #15133, #19473, #21954, .T. ) ;
#6002=ORIENTED_EDGE ( 'NONE', *, *, #5951, .F. ) ;
#6003=EDGE_CURVE ( 'NONE', #2081, #19473, #16194, .T. ) ;
#6006=EDGE_LOOP ( 'NONE', ( #10670, #3178, #2837, #10695, #4977, #21848, #5611, #11586, #1446 ) ) ;
#6014=DIRECTION ( 'NONE',  ( 3.099353312215989243E-62, 1.872670541876879671E-92, -1.000000000000000000 ) ) ;
#6068=CARTESIAN_POINT ( 'NONE',  ( -27.00000000000000000, -31.09999999999999787, 21.50000000000000000 ) ) ;
#6216=AXIS2_PLACEMENT_3D ( 'NONE', #9238, #21922, #5654 ) ;
#6226=CARTESIAN_POINT ( 'NONE',  ( -2.499999999999973799, 4.120723506284736299E-15, 2.500000000000000000 ) ) ;
#6295=ORIENTED_EDGE ( 'NONE', *, *, #6003, .T. ) ;
#6321=ORIENTED_EDGE ( 'NONE', *, *, #18467, .F. ) ;
#6326=VERTEX_POINT ( 'NONE', #19272 ) ;
#6335=CARTESIAN_POINT ( 'NONE',  ( -27.00000000000000000, -27.34999999999999787, 6.250000000000000000 ) ) ;
#6352=FACE_OUTER_BOUND ( 'NONE', #223, .T. ) ;
#6356=DIRECTION ( 'NONE',  ( 0.8846153846153629319, -0.4663213712685850276, 0.000000000000000000 ) ) ;
#6357=EDGE_CURVE ( 'NONE', #19233, #4824, #9046, .T. ) ;
#6374=CARTESIAN_POINT ( 'NONE',  ( -1.540112692620030144, -27.34999999999999787, 5.000000000000000000 ) ) ;
#6381=EDGE_CURVE ( 'NONE', #5291, #17008, #121, .T. ) ;
#6407=ORIENTED_EDGE ( 'NONE', *, *, #21724, .T. ) ;
#6444=DIRECTION ( 'NONE',  ( 0.000000000000000000, 0.000000000000000000, -1.000000000000000000 ) ) ;
#6469=ORIENTED_EDGE ( 'NONE', *, *, #21724, .F. ) ;
#6484=CARTESIAN_POINT ( 'NONE',  ( 2.664535259100379799E-14, -1.554450629062440126E-15, 5.000000000000000000 ) ) ;
#6504=DIRECTION ( 'NONE',  ( 1.000000000000000000, 3.099353312215988811E-62, 0.000000000000000000 ) ) ;
#6522=VERTEX_POINT ( 'NONE', #20550 ) ;
#6526=VERTEX_POINT ( 'NONE', #20436 ) ;
#6545=EDGE_CURVE ( 'NONE', #12545, #3638, #22450, .T. ) ;
#6560=VECTOR ( 'NONE', #7906, 1000.000000000000000 ) ;
#6563=VERTEX_POINT ( 'NONE', #9764 ) ;
#6573=AXIS2_PLACEMENT_3D ( 'NONE', #8273, #1121, #15856 ) ;
#6581=CIRCLE ( 'NONE', #1622, 2.500000000000001776 ) ;
#6588=FACE_OUTER_BOUND ( 'NONE', #21477, .T. ) ;
#6590=CARTESIAN_POINT ( 'NONE',  ( -27.00000000000000000, -20.00000000000000000, 2.500000000000000000 ) ) ;
#6648=ORIENTED_EDGE ( 'NONE', *, *, #17255, .F. ) ;
#6668=EDGE_CURVE ( 'NONE', #4824, #6526, #9242, .T. ) ;
#6675=AXIS2_PLACEMENT_3D ( 'NONE', #3405, #8763, #3533 ) ;
#6702=CARTESIAN_POINT ( 'NONE',  ( 2.664535259100379799E-14, -1.554450629062440126E-15, 2.500000000000000000 ) ) ;
#6709=FACE_OUTER_BOUND ( 'NONE', #2761, .T. ) ;
#6711=LINE ( 'NONE', #8252, #14106 ) ;
#6749=CARTESIAN_POINT ( 'NONE',  ( -24.50000000000000000, -30.47499999999999787, 21.50000000000000000 ) ) ;
#6774=ORIENTED_EDGE ( 'NONE', *, *, #14739, .F. ) ;
#6836=LINE ( 'NONE', #1351, #18962 ) ;
#6862=LINE ( 'NONE', #6749, #3866 ) ;
#6958=LINE ( 'NONE', #13838, #19436 ) ;
#6980=AXIS2_PLACEMENT_3D ( 'NONE', #11249, #13361, #19154 ) ;
#7070=ORIENTED_EDGE ( 'NONE', *, *, #22705, .T. ) ;
#7075=CARTESIAN_POINT ( 'NONE',  ( 6.500000000000000000, -17.30000000000000071, 5.000000000000000000 ) ) ;
#7116=DIRECTION ( 'NONE',  ( -2.270069654138870255E-15, -1.000000000000000000, -7.035747901516317327E-77 ) ) ;
#7124=AXIS2_PLACEMENT_3D ( 'NONE', #512, #5866, #20464 ) ;
#7179=DIRECTION ( 'NONE',  ( -1.000000000000000000, 2.270069654138870255E-15, -3.099353312215988811E-62 ) ) ;
#7189=DIRECTION ( 'NONE',  ( 0.8846153846154060085, -0.4663213712685030377, 0.000000000000000000 ) ) ;
#7191=ADVANCED_FACE ( 'NONE', ( #19194 ), #15622, .T. ) ;
#7209=FACE_OUTER_BOUND ( 'NONE', #18973, .T. ) ;
#7294=ORIENTED_EDGE ( 'NONE', *, *, #8856, .F. ) ;
#7359=CIRCLE ( 'NONE', #6980, 3.499999999999999556 ) ;
#7360=ORIENTED_EDGE ( 'NONE', *, *, #3915, .F. ) ;
#7386=CARTESIAN_POINT ( 'NONE',  ( -27.00000000000000000, -31.09999999999999787, 19.00000000000000000 ) ) ;
#7456=CARTESIAN_POINT ( 'NONE',  ( 5.000000000000000000, -31.09999999999999787, 5.000000000000000000 ) ) ;
#7480=ADVANCED_FACE ( 'NONE', ( #8970 ), #1943, .T. ) ;
#7542=DIRECTION ( 'NONE',  ( -3.099353312215989243E-62, 1.001855809244433740E-92, 1.000000000000000000 ) ) ;
#7545=CARTESIAN_POINT ( 'NONE',  ( -1.262685242559879909E-14, -17.30000000000000071, 2.500000000000000000 ) ) ;
#7577=ORIENTED_EDGE ( 'NONE', *, *, #20084, .T. ) ;
#7579=DIRECTION ( 'NONE',  ( 1.169815979547696263E-44, 1.000000000000000000, 5.153216234642169651E-30 ) ) ;
#7687=DIRECTION ( 'NONE',  ( -3.099353312215988811E-62, -9.818186930595456717E-93, 1.000000000000000000 ) ) ;
#7700=DIRECTION ( 'NONE',  ( 2.270069654138870255E-15, 1.000000000000000000, 7.035747901516317327E-77 ) ) ;
#7868=EDGE_LOOP ( 'NONE', ( #18893, #8727, #7294, #18801 ) ) ;
#7891=AXIS2_PLACEMENT_3D ( 'NONE', #12682, #23102, #5088 ) ;
#7906=DIRECTION ( 'NONE',  ( -3.099353312215988811E-62, 0.000000000000000000, 1.000000000000000000 ) ) ;
#7954=LINE ( 'NONE', #22426, #12957 ) ;
#7983=EDGE_LOOP ( 'NONE', ( #1666, #18303, #15551, #2870, #12029, #12411, #20046, #7360 ) ) ;
#7998=CYLINDRICAL_SURFACE ( 'NONE', #18322, 6.500000000000000888 ) ;
#8027=ORIENTED_EDGE ( 'NONE', *, *, #4301, .T. ) ;
#8038=CARTESIAN_POINT ( 'NONE',  ( -24.50000000000000000, -28.60000000000000142, 21.50000000000000000 ) ) ;
#8055=LINE ( 'NONE', #15291, #23200 ) ;
#8084=CYLINDRICAL_SURFACE ( 'NONE', #21012, 2.500000000000001776 ) ;
#8085=LINE ( 'NONE', #10107, #93 ) ;
#8100=AXIS2_PLACEMENT_3D ( 'NONE', #21353, #15999, #21223 ) ;
#8187=DIRECTION ( 'NONE',  ( -0.7194962871189621856, -0.6944962871189651610, -2.229973200609260484E-62 ) ) ;
#8221=APPLICATION_CONTEXT ( 'configuration controlled 3d designs of mechanical parts and assemblies' ) ;
#8226=ORIENTED_EDGE ( 'NONE', *, *, #3541, .T. ) ;
#8252=CARTESIAN_POINT ( 'NONE',  ( 5.750000000000129674, -20.33108891324529921, 2.500000000000000000 ) ) ;
#8261=DIRECTION ( 'NONE',  ( -3.099353312215988811E-62, 0.000000000000000000, 1.000000000000000000 ) ) ;
#8273=CARTESIAN_POINT ( 'NONE',  ( -20.00000000000000000, -20.00000000000000000, 2.500000000000000000 ) ) ;
#8280=LINE ( 'NONE', #6374, #17097 ) ;
#8299=ADVANCED_FACE ( 'NONE', ( #13988 ), #8765, .T. ) ;
#8301=VERTEX_POINT ( 'NONE', #8418 ) ;
#8359=CARTESIAN_POINT ( 'NONE',  ( 2.664535259100379799E-14, 6.659954201878760116E-16, 2.500000000000000000 ) ) ;
#8376=ORIENTED_EDGE ( 'NONE', *, *, #3571, .F. ) ;
#8418=CARTESIAN_POINT ( 'NONE',  ( -24.50000000000000000, -31.09999999999999787, 21.50000000000000000 ) ) ;
#8424=LINE ( 'NONE', #4737, #1194 ) ;
#8445=AXIS2_PLACEMENT_3D ( 'NONE', #13973, #12434, #19666 ) ;
#8455=CIRCLE ( 'NONE', #837, 6.499999999999998224 ) ;
#8474=EDGE_CURVE ( 'NONE', #17116, #3741, #15309, .T. ) ;
#8490=AXIS2_PLACEMENT_3D ( 'NONE', #16205, #23436, #7189 ) ;
#8497=ORIENTED_EDGE ( 'NONE', *, *, #10067, .F. ) ;
#8522=DIRECTION ( 'NONE',  ( -0.6944962871189651610, 0.7194962871189621856, -2.152489367803870976E-62 ) ) ;
#8585=ORIENTED_EDGE ( 'NONE', *, *, #8683, .T. ) ;
#8620=VECTOR ( 'NONE', #13828, 1000.000000000000000 ) ;
#8641=VERTEX_POINT ( 'NONE', #8038 ) ;
#8655=ORIENTED_EDGE ( 'NONE', *, *, #10530, .F. ) ;
#8683=EDGE_CURVE ( 'NONE', #6563, #17008, #17597, .T. ) ;
#8721=CYLINDRICAL_SURFACE ( 'NONE', #12996, 3.499999999999999556 ) ;
#8727=ORIENTED_EDGE ( 'NONE', *, *, #4318, .T. ) ;
#8763=DIRECTION ( 'NONE',  ( -3.099353312215989243E-62, -1.872670541876879671E-92, 1.000000000000000000 ) ) ;
#8765=PLANE ( 'NONE',  #8100 ) ;
#8826=VECTOR ( 'NONE', #988, 1000.000000000000000 ) ;
#8832=AXIS2_PLACEMENT_3D ( 'NONE', #21152, #3222, #22571 ) ;
#8854=CIRCLE ( 'NONE', #5812, 7.000000000000000000 ) ;
#8856=EDGE_CURVE ( 'NONE', #3741, #17116, #138, .T. ) ;
#8909=VERTEX_POINT ( 'NONE', #16546 ) ;
#8939=EDGE_CURVE ( 'NONE', #12850, #3176, #13442, .T. ) ;
#8950=ADVANCED_FACE ( 'NONE', ( #10895 ), #5403, .F. ) ;
#8970=FACE_OUTER_BOUND ( 'NONE', #19238, .T. ) ;
#8973=VECTOR ( 'NONE', #7116, 1000.000000000000000 ) ;
#8981=CARTESIAN_POINT ( 'NONE',  ( 2.500000000000026645, -7.535786464196452844E-15, 5.000000000000000000 ) ) ;
#9014=CARTESIAN_POINT ( 'NONE',  ( -2.500000000000012434, -17.29999999999999361, 5.000000000000000000 ) ) ;
#9021=CIRCLE ( 'NONE', #15444, 7.000000000000000000 ) ;
#9046=LINE ( 'NONE', #1674, #16072 ) ;
#9078=PRODUCT_DEFINITION ( 'UNKNOWN', '', #19087, #163 ) ;
#9082=DIRECTION ( 'NONE',  ( 3.099353312215989243E-62, 0.000000000000000000, -1.000000000000000000 ) ) ;
#9087=DIRECTION ( 'NONE',  ( -1.000000000000000000, 2.775557561562891351E-15, 0.000000000000000000 ) ) ;
#9102=DIRECTION ( 'NONE',  ( -1.000000000000000000, 1.982541115402065307E-15, 0.000000000000000000 ) ) ;
#9196=CARTESIAN_POINT ( 'NONE',  ( -1.262685242559879909E-14, -17.30000000000000071, 2.500000000000000000 ) ) ;
#9222=PLANE ( 'NONE',  #20959 ) ;
#9236=ORIENTED_EDGE ( 'NONE', *, *, #15383, .T. ) ;
#9238=CARTESIAN_POINT ( 'NONE',  ( 2.664535259100379799E-14, -1.554450629062440126E-15, 5.000000000000000000 ) ) ;
#9242=CIRCLE ( 'NONE', #22510, 2.500000000000000888 ) ;
#9280=ADVANCED_FACE ( 'NONE', ( #6588 ), #19058, .F. ) ;
#9387=LINE ( 'NONE', #12724, #896 ) ;
#9397=ORIENTED_EDGE ( 'NONE', *, *, #16655, .F. ) ;
#9405=AXIS2_PLACEMENT_3D ( 'NONE', #23233, #17897, #11019 ) ;
#9408=ORIENTED_EDGE ( 'NONE', *, *, #19414, .T. ) ;
#9430=VERTEX_POINT ( 'NONE', #10977 ) ;
#9447=ORIENTED_EDGE ( 'NONE', *, *, #555, .F. ) ;
#9528=VECTOR ( 'NONE', #21660, 1000.000000000000000 ) ;
#9539=CARTESIAN_POINT ( 'NONE',  ( 5.000000000000000000, -27.34999999999999787, 2.500000000000000000 ) ) ;
#9551=ORIENTED_EDGE ( 'NONE', *, *, #16882, .T. ) ;
#9598=AXIS2_PLACEMENT_3D ( 'NONE', #10841, #5235, #12831 ) ;
#9602=VECTOR ( 'NONE', #23457, 1000.000000000000000 ) ;
#9658=CIRCLE ( 'NONE', #2438, 2.500000000000000888 ) ;
#9678=FACE_OUTER_BOUND ( 'NONE', #15642, .T. ) ;
#9723=EDGE_CURVE ( 'NONE', #20176, #6526, #20330, .T. ) ;
#9725=ORIENTED_EDGE ( 'NONE', *, *, #17238, .T. ) ;
#9764=CARTESIAN_POINT ( 'NONE',  ( 2.499999999999987566, -17.30000000000000782, 5.000000000000000000 ) ) ;
#9787=CARTESIAN_POINT ( 'NONE',  ( -27.00000000000000000, -31.09999999999999787, 6.250000000000000000 ) ) ;
#9792=EDGE_CURVE ( 'NONE', #18951, #11427, #22002, .T. ) ;
#9801=CARTESIAN_POINT ( 'NONE',  ( 5.000000000000000000, -23.36217782649100272, 2.500000000000000000 ) ) ;
#9890=AXIS2_PLACEMENT_3D ( 'NONE', #13702, #2784, #21171 ) ;
#9895=EDGE_LOOP ( 'NONE', ( #994, #14212, #9725, #3828 ) ) ;
#9903=CARTESIAN_POINT ( 'NONE',  ( 11.50000000000000000, -23.36217782649120167, 2.500000000000000000 ) ) ;
#9920=VECTOR ( 'NONE', #2341, 1000.000000000000000 ) ;
#9959=LINE ( 'NONE', #10079, #9920 ) ;
#9962=AXIS2_PLACEMENT_3D ( 'NONE', #5914, #7579, #16706 ) ;
#9969=EDGE_CURVE ( 'NONE', #1465, #3741, #16037, .T. ) ;
#9998=DIRECTION ( 'NONE',  ( 2.270069654138865127E-15, 1.000000000000000000, -4.543838814073030634E-30 ) ) ;
#10000=EDGE_LOOP ( 'NONE', ( #17522, #13992 ) ) ;
#10067=EDGE_CURVE ( 'NONE', #16708, #18951, #8280, .T. ) ;
#10079=CARTESIAN_POINT ( 'NONE',  ( 5.000000000000000000, -23.36217782649100272, 2.500000000000000000 ) ) ;
#10087=FACE_BOUND ( 'NONE', #13876, .T. ) ;
#10107=CARTESIAN_POINT ( 'NONE',  ( -1.540112692620030144, -27.34999999999999787, 2.500000000000000000 ) ) ;
#10132=ORIENTED_EDGE ( 'NONE', *, *, #14272, .F. ) ;
#10136=ORIENTED_EDGE ( 'NONE', *, *, #3748, .T. ) ;
#10177=CIRCLE ( 'NONE', #23411, 1.250000000000000222 ) ;
#10185=SHAPE_REPRESENTATION_RELATIONSHIP ( 'NONE' , 'NONE' ,  #17646, #3978 ) ;
#10206=ORIENTED_EDGE ( 'NONE', *, *, #5951, .T. ) ;
#10309=EDGE_CURVE ( 'NONE', #21101, #6563, #19551, .T. ) ;
#10335=EDGE_LOOP ( 'NONE', ( #2462, #8655, #1960, #1125 ) ) ;
#10354=AXIS2_PLACEMENT_3D ( 'NONE', #19265, #14028, #19497 ) ;
#10414=LINE ( 'NONE', #2906, #22082 ) ;
#10422=EDGE_CURVE ( 'NONE', #2924, #16237, #16213, .T. ) ;
#10530=EDGE_CURVE ( 'NONE', #5291, #21101, #23169, .T. ) ;
#10563=ADVANCED_FACE ( 'NONE', ( #5523 ), #395, .T. ) ;
#10575=ORIENTED_EDGE ( 'NONE', *, *, #9723, .F. ) ;
#10614=LINE ( 'NONE', #16055, #17893 ) ;
#10621=VECTOR ( 'NONE', #7179, 1000.000000000000000 ) ;
#10656=CARTESIAN_POINT ( 'NONE',  ( 2.499999999999987566, -17.30000000000000782, 2.500000000000000000 ) ) ;
#10670=ORIENTED_EDGE ( 'NONE', *, *, #10067, .T. ) ;
#10695=ORIENTED_EDGE ( 'NONE', *, *, #20154, .F. ) ;
#10734=CARTESIAN_POINT ( 'NONE',  ( -2.500000000000012434, -17.29999999999999361, 2.500000000000000000 ) ) ;
#10741=EDGE_CURVE ( 'NONE', #15256, #1296, #21415, .T. ) ;
#10751=ADVANCED_FACE ( 'NONE', ( #6709 ), #21175, .T. ) ;
#10764=DIRECTION ( 'NONE',  ( 0.000000000000000000, 0.000000000000000000, -1.000000000000000000 ) ) ;
#10823=CARTESIAN_POINT ( 'NONE',  ( 6.500000000000000000, -17.30000000000000071, 2.500000000000000000 ) ) ;
#10841=CARTESIAN_POINT ( 'NONE',  ( 2.499999999999970246, -31.09999999999999787, 19.00000000000000000 ) ) ;
#10851=LINE ( 'NONE', #1786, #21044 ) ;
#10873=VERTEX_POINT ( 'NONE', #13705 ) ;
#10895=FACE_OUTER_BOUND ( 'NONE', #21427, .T. ) ;
#10904=ORIENTED_EDGE ( 'NONE', *, *, #9792, .F. ) ;
#10936=ORIENTED_EDGE ( 'NONE', *, *, #289, .F. ) ;
#10953=DIRECTION ( 'NONE',  ( -0.6944962871189153120, 0.7194962871190101472, 0.000000000000000000 ) ) ;
#10958=EDGE_LOOP ( 'NONE', ( #9408, #3865, #1626, #4425 ) ) ;
#10977=CARTESIAN_POINT ( 'NONE',  ( -24.86147400983239919, -14.96352599016710094, 2.500000000000000000 ) ) ;
#11008=CARTESIAN_POINT ( 'NONE',  ( 2.499999999999970246, -31.09999999999999787, 19.00000000000000000 ) ) ;
#11019=DIRECTION ( 'NONE',  ( -1.000000000000000000, 2.775557561562891351E-15, 0.000000000000000000 ) ) ;
#11095=CIRCLE ( 'NONE', #75, 2.500000000000001776 ) ;
#11135=DIRECTION ( 'NONE',  ( 0.7071067811865476838, -1.387778780781444689E-15, 0.7071067811865473507 ) ) ;
#11137=EDGE_LOOP ( 'NONE', ( #6295, #6002, #4695, #15324 ) ) ;
#11144=CARTESIAN_POINT ( 'NONE',  ( -8.080225385240009217, -15.72171916155420313, 2.500000000000000000 ) ) ;
#11149=MECHANICAL_CONTEXT ( 'NONE', #8221, 'mechanical' ) ;
#11167=ORIENTED_EDGE ( 'NONE', *, *, #16451, .F. ) ;
#11176=AXIS2_PLACEMENT_3D ( 'NONE', #21389, #17719, #21150 ) ;
#11199=CARTESIAN_POINT ( 'NONE',  ( -20.00000000000000000, -20.00000000000000000, 5.000000000000000000 ) ) ;
#11230=DIRECTION ( 'NONE',  ( -0.6944962871189153120, 0.7194962871190101472, 0.000000000000000000 ) ) ;
#11249=CARTESIAN_POINT ( 'NONE',  ( -20.00000000000000000, -20.00000000000000000, 2.500000000000000000 ) ) ;
#11269=EDGE_LOOP ( 'NONE', ( #23036, #10136 ) ) ;
#11308=VERTEX_POINT ( 'NONE', #15809 ) ;
#11332=DIRECTION ( 'NONE',  ( 3.099353312215988811E-62, 0.000000000000000000, -1.000000000000000000 ) ) ;
#11337=DIRECTION ( 'NONE',  ( -2.270069654138865127E-15, -1.000000000000000000, -4.543838814073030634E-30 ) ) ;
#11427=VERTEX_POINT ( 'NONE', #1890 ) ;
#11451=EDGE_LOOP ( 'NONE', ( #3313, #19530, #9236, #20915 ) ) ;
#11510=VERTEX_POINT ( 'NONE', #218 ) ;
#11527=VERTEX_POINT ( 'NONE', #19955 ) ;
#11578=EDGE_CURVE ( 'NONE', #9430, #687, #9021, .T. ) ;
#11586=ORIENTED_EDGE ( 'NONE', *, *, #19414, .F. ) ;
#11635=DIRECTION ( 'NONE',  ( -0.7071067811865475727, 1.387778780781445281E-15, 0.7071067811865475727 ) ) ;
#11661=CARTESIAN_POINT ( 'NONE',  ( 2.499999999999970246, -28.60000000000000142, 19.00000000000000000 ) ) ;
#11686=ADVANCED_FACE ( 'NONE', ( #4149 ), #3923, .F. ) ;
#11722=ORIENTED_EDGE ( 'NONE', *, *, #17238, .F. ) ;
#11727=DIRECTION ( 'NONE',  ( -3.099353312215989243E-62, 1.403547063447849893E-77, 1.000000000000000000 ) ) ;
#11797=AXIS2_PLACEMENT_3D ( 'NONE', #21036, #19257, #23034 ) ;
#11909=EDGE_CURVE ( 'NONE', #687, #11308, #2208, .T. ) ;
#11944=AXIS2_PLACEMENT_3D ( 'NONE', #11199, #20310, #22193 ) ;
#11977=DIRECTION ( 'NONE',  ( -1.000000000000000000, 2.270069654138870255E-15, 0.000000000000000000 ) ) ;
#12004=DIRECTION ( 'NONE',  ( -3.099353312215988811E-62, 0.000000000000000000, 1.000000000000000000 ) ) ;
#12029=ORIENTED_EDGE ( 'NONE', *, *, #13008, .T. ) ;
#12057=FACE_OUTER_BOUND ( 'NONE', #7868, .T. ) ;
#12059=CIRCLE ( 'NONE', #1417, 3.750000000000000000 ) ;
#12073=DIRECTION ( 'NONE',  ( -1.000000000000000000, 1.982541115402065307E-15, 0.000000000000000000 ) ) ;
#12107=ADVANCED_FACE ( 'NONE', ( #898 ), #23083, .T. ) ;
#12129=EDGE_LOOP ( 'NONE', ( #10575, #5557, #3630, #4159 ) ) ;
#12145=EDGE_LOOP ( 'NONE', ( #5697, #21971, #11722, #1900, #6774, #6407, #22442, #20765 ) ) ;
#12167=CIRCLE ( 'NONE', #15172, 2.500000000000001776 ) ;
#12169=ADVANCED_FACE ( 'NONE', ( #14077 ), #19195, .T. ) ;
#12177=DIRECTION ( 'NONE',  ( -3.099353312215989243E-62, 0.000000000000000000, 1.000000000000000000 ) ) ;
#12183=DIRECTION ( 'NONE',  ( 1.000000000000000000, -2.611676738638919574E-15, 0.000000000000000000 ) ) ;
#12203=CIRCLE ( 'NONE', #17111, 2.500000000000000888 ) ;
#12204=CARTESIAN_POINT ( 'NONE',  ( -11.00000000000000000, -27.34999999999999787, 6.250000000000000000 ) ) ;
#12214=CARTESIAN_POINT ( 'NONE',  ( 5.750000000000129674, -20.33108891324529921, 2.500000000000000000 ) ) ;
#12294=CARTESIAN_POINT ( 'NONE',  ( 5.750000000000129674, -20.33108891324529921, 5.000000000000000000 ) ) ;
#12388=PLANE ( 'NONE',  #9962 ) ;
#12404=AXIS2_PLACEMENT_3D ( 'NONE', #3705, #1566, #5495 ) ;
#12411=ORIENTED_EDGE ( 'NONE', *, *, #6003, .F. ) ;
#12429=ORIENTED_EDGE ( 'NONE', *, *, #20373, .T. ) ;
#12434=DIRECTION ( 'NONE',  ( -3.099353312215989243E-62, 9.554441540188157279E-93, 1.000000000000000000 ) ) ;
#12452=AXIS2_PLACEMENT_3D ( 'NONE', #20657, #18654, #2371 ) ;
#12495=DIRECTION ( 'NONE',  ( -2.270069654138865127E-15, -1.000000000000000000, 4.574083617919690056E-30 ) ) ;
#12544=DIRECTION ( 'NONE',  ( -2.270069654138865127E-15, -1.000000000000000000, -4.543838814073030634E-30 ) ) ;
#12545=VERTEX_POINT ( 'NONE', #9801 ) ;
#12606=VERTEX_POINT ( 'NONE', #3002 ) ;
#12635=VECTOR ( 'NONE', #8261, 1000.000000000000000 ) ;
#12640=CARTESIAN_POINT ( 'NONE',  ( -23.50000000000000000, -19.99999999999999289, 2.500000000000000000 ) ) ;
#12667=CARTESIAN_POINT ( 'NONE',  ( -20.00000000000000000, -20.00000000000000000, 2.500000000000000000 ) ) ;
#12679=FACE_BOUND ( 'NONE', #10000, .T. ) ;
#12680=AXIS2_PLACEMENT_3D ( 'NONE', #14309, #9082, #12772 ) ;
#12682=CARTESIAN_POINT ( 'NONE',  ( 5.000000000000000000, -29.85000000000000142, 12.00000000000000000 ) ) ;
#12715=ADVANCED_FACE ( 'NONE', ( #12057 ), #19283, .F. ) ;
#12724=CARTESIAN_POINT ( 'NONE',  ( 5.000000000000000000, -28.60000000000000142, 2.500000000000000000 ) ) ;
#12739=AXIS2_PLACEMENT_3D ( 'NONE', #2569, #13380, #415 ) ;
#12754=ORIENTED_EDGE ( 'NONE', *, *, #32, .T. ) ;
#12772=DIRECTION ( 'NONE',  ( 1.000000000000000000, -2.611676738638919574E-15, 0.000000000000000000 ) ) ;
#12831=DIRECTION ( 'NONE',  ( 0.7071067811865476838, -1.387778780781444689E-15, 0.7071067811865473507 ) ) ;
#12832=VERTEX_POINT ( 'NONE', #12294 ) ;
#12845=EDGE_CURVE ( 'NONE', #8909, #5287, #21627, .T. ) ;
#12850=VERTEX_POINT ( 'NONE', #16069 ) ;
#12852=CYLINDRICAL_SURFACE ( 'NONE', #12404, 1.250000000000000222 ) ;
#12886=CARTESIAN_POINT ( 'NONE',  ( 6.500000000000000000, -17.30000000000000071, 5.000000000000000000 ) ) ;
#12895=CARTESIAN_POINT ( 'NONE',  ( -26.26776695296636888, -28.59999999999999787, 20.76776695296636888 ) ) ;
#12957=VECTOR ( 'NONE', #8187, 999.9999999999998863 ) ;
#12996=AXIS2_PLACEMENT_3D ( 'NONE', #17517, #19295, #12073 ) ;
#13008=EDGE_CURVE ( 'NONE', #4824, #19473, #4055, .T. ) ;
#13046=ORIENTED_EDGE ( 'NONE', *, *, #22449, .F. ) ;
#13115=CIRCLE ( 'NONE', #6675, 2.500000000000000000 ) ;
#13202=FACE_BOUND ( 'NONE', #4291, .T. ) ;
#13241=DIRECTION ( 'NONE',  ( 2.270069654138870255E-15, 1.000000000000000000, 7.035747901516317327E-77 ) ) ;
#13246=CARTESIAN_POINT ( 'NONE',  ( 2.499999999999970246, -30.47499999999999787, 19.00000000000000000 ) ) ;
#13255=( NAMED_UNIT ( * ) PLANE_ANGLE_UNIT ( ) SI_UNIT ( $, .RADIAN. ) );
#13361=DIRECTION ( 'NONE',  ( -3.099353312215989243E-62, 9.554441540188157279E-93, 1.000000000000000000 ) ) ;
#13372=ORIENTED_EDGE ( 'NONE', *, *, #10741, .T. ) ;
#13380=DIRECTION ( 'NONE',  ( 0.000000000000000000, 0.000000000000000000, 1.000000000000000000 ) ) ;
#13405=ADVANCED_FACE ( 'NONE', ( #3648 ), #1856, .F. ) ;
#13438=DIRECTION ( 'NONE',  ( 3.099353312215989243E-62, -1.403547063447849893E-77, -1.000000000000000000 ) ) ;
#13442=CIRCLE ( 'NONE', #12680, 6.500000000000000000 ) ;
#13445=CIRCLE ( 'NONE', #11176, 2.500000000000000888 ) ;
#13553=DIRECTION ( 'NONE',  ( -1.000000000000000000, 2.270069654138870255E-15, -3.099353312215989243E-62 ) ) ;
#13559=CYLINDRICAL_SURFACE ( 'NONE', #8832, 2.500000000000000000 ) ;
#13567=CARTESIAN_POINT ( 'NONE',  ( -20.00000000000000000, -20.00000000000000000, 5.000000000000000000 ) ) ;
#13598=DIRECTION ( 'NONE',  ( 0.7071067811865476838, -1.387778780781444689E-15, 0.7071067811865473507 ) ) ;
#13679=PRODUCT_DEFINITION_SHAPE ( 'NONE', 'NONE',  #9078 ) ;
#13702=CARTESIAN_POINT ( 'NONE',  ( -1.262685242559879909E-14, -17.30000000000000071, 2.500000000000000000 ) ) ;
#13705=CARTESIAN_POINT ( 'NONE',  ( 5.000000000000000000, -28.60000000000000142, 19.00000000000000000 ) ) ;
#13713=DIRECTION ( 'NONE',  ( 2.270069654138865127E-15, 1.000000000000000000, -4.543838814073030634E-30 ) ) ;
#13828=DIRECTION ( 'NONE',  ( -2.270069654138870255E-15, -1.000000000000000000, -7.035747901516317327E-77 ) ) ;
#13838=CARTESIAN_POINT ( 'NONE',  ( -27.00000000000000000, -28.60000000000000142, 2.500000000000000000 ) ) ;
#13840=ORIENTED_EDGE ( 'NONE', *, *, #530, .F. ) ;
#13876=EDGE_LOOP ( 'NONE', ( #5477, #15310 ) ) ;
#13914=FACE_OUTER_BOUND ( 'NONE', #10335, .T. ) ;
#13941=DIRECTION ( 'NONE',  ( 2.270069654138865127E-15, 1.000000000000000000, -4.543838814073030634E-30 ) ) ;
#13952=ORIENTED_EDGE ( 'NONE', *, *, #20170, .F. ) ;
#13973=CARTESIAN_POINT ( 'NONE',  ( -20.00000000000000000, -20.00000000000000000, 2.500000000000000000 ) ) ;
#13978=ORIENTED_EDGE ( 'NONE', *, *, #555, .T. ) ;
#13988=FACE_OUTER_BOUND ( 'NONE', #7983, .T. ) ;
#13992=ORIENTED_EDGE ( 'NONE', *, *, #1252, .T. ) ;
#14028=DIRECTION ( 'NONE',  ( -2.270069654138865127E-15, -1.000000000000000000, -4.543838814073030634E-30 ) ) ;
#14052=CYLINDRICAL_SURFACE ( 'NONE', #22631, 6.500000000000000000 ) ;
#14057=EDGE_LOOP ( 'NONE', ( #10206, #19731, #4268, #4043, #20630, #4588, #23016, #23226 ) ) ;
#14077=FACE_OUTER_BOUND ( 'NONE', #11451, .T. ) ;
#14090=LINE ( 'NONE', #3175, #20628 ) ;
#14106=VECTOR ( 'NONE', #21177, 1000.000000000000000 ) ;
#14151=ORIENTED_EDGE ( 'NONE', *, *, #20084, .F. ) ;
#14207=ADVANCED_FACE ( 'NONE', ( #19176 ), #14052, .T. ) ;
#14212=ORIENTED_EDGE ( 'NONE', *, *, #3915, .T. ) ;
#14272=EDGE_CURVE ( 'NONE', #687, #15133, #22708, .T. ) ;
#14309=CARTESIAN_POINT ( 'NONE',  ( 2.664535259100379799E-14, 6.659954201878760116E-16, 5.000000000000000000 ) ) ;
#14314=CARTESIAN_POINT ( 'NONE',  ( -24.50000000000000000, -30.47499999999999787, 19.00000000000000000 ) ) ;
#14339=ADVANCED_FACE ( 'NONE', ( #17853 ), #12852, .F. ) ;
#14393=CARTESIAN_POINT ( 'NONE',  ( -16.50000000000000000, -20.00000000000000711, 2.500000000000000000 ) ) ;
#14471=APPLICATION_CONTEXT ( 'configuration controlled 3d designs of mechanical parts and assemblies' ) ;
#14571=PLANE ( 'NONE',  #7891 ) ;
#14672=DIRECTION ( 'NONE',  ( 1.000000000000000000, 3.099353312215988811E-62, 0.000000000000000000 ) ) ;
#14721=AXIS2_PLACEMENT_3D ( 'NONE', #6702, #20707, #4907 ) ;
#14739=EDGE_CURVE ( 'NONE', #16163, #2081, #12059, .T. ) ;
#14780=LINE ( 'NONE', #5756, #21000 ) ;
#14783=ORIENTED_EDGE ( 'NONE', *, *, #20154, .T. ) ;
#14970=PLANE ( 'NONE',  #274 ) ;
#15086=DIRECTION ( 'NONE',  ( -0.7071067811865475727, 1.387778780781445281E-15, 0.7071067811865475727 ) ) ;
#15133=VERTEX_POINT ( 'NONE', #20307 ) ;
#15153=AXIS2_PLACEMENT_3D ( 'NONE', #7545, #1833, #9087 ) ;
#15154=DIRECTION ( 'NONE',  ( 2.270069654138870255E-15, 1.000000000000000000, 7.035747901516317327E-77 ) ) ;
#15161=ORIENTED_EDGE ( 'NONE', *, *, #9723, .T. ) ;
#15172=AXIS2_PLACEMENT_3D ( 'NONE', #5238, #12495, #19960 ) ;
#15196=VECTOR ( 'NONE', #7687, 1000.000000000000000 ) ;
#15220=EDGE_CURVE ( 'NONE', #15757, #12850, #8424, .T. ) ;
#15256=VERTEX_POINT ( 'NONE', #20884 ) ;
#15277=DIRECTION ( 'NONE',  ( -1.000000000000000000, 2.270069654138870255E-15, 0.000000000000000000 ) ) ;
#15291=CARTESIAN_POINT ( 'NONE',  ( -27.00000000000000000, -31.09999999999999787, 21.50000000000000000 ) ) ;
#15309=CIRCLE ( 'NONE', #6216, 2.500000000000000000 ) ;
#15310=ORIENTED_EDGE ( 'NONE', *, *, #17683, .T. ) ;
#15316=CARTESIAN_POINT ( 'NONE',  ( 2.499999999999970246, -30.47499999999999787, 19.00000000000000000 ) ) ;
#15324=ORIENTED_EDGE ( 'NONE', *, *, #14739, .T. ) ;
#15325=CARTESIAN_POINT ( 'NONE',  ( 11.50000000000000000, -23.36217782649120167, 2.500000000000000000 ) ) ;
#15344=ORIENTED_EDGE ( 'NONE', *, *, #4874, .T. ) ;
#15349=DIRECTION ( 'NONE',  ( -3.099353312215989243E-62, 1.308200680535015858E-77, 1.000000000000000000 ) ) ;
#15375=ORIENTED_EDGE ( 'NONE', *, *, #20360, .T. ) ;
#15383=EDGE_CURVE ( 'NONE', #15757, #9430, #7954, .T. ) ;
#15394=DIRECTION ( 'NONE',  ( 2.270069654138865127E-15, 1.000000000000000000, 4.574083617919690056E-30 ) ) ;
#15401=DIRECTION ( 'NONE',  ( 1.000000000000000000, -2.270069654138870255E-15, 3.099353312215988811E-62 ) ) ;
#15443=ORIENTED_EDGE ( 'NONE', *, *, #32, .F. ) ;
#15444=AXIS2_PLACEMENT_3D ( 'NONE', #3677, #23383, #10953 ) ;
#15473=DIRECTION ( 'NONE',  ( -1.000000000000000000, 2.270069654138870255E-15, -3.099353312215989243E-62 ) ) ;
#15486=AXIS2_PLACEMENT_3D ( 'NONE', #12204, #22972, #17530 ) ;
#15514=AXIS2_PLACEMENT_3D ( 'NONE', #13246, #13713, #13598 ) ;
#15551=ORIENTED_EDGE ( 'NONE', *, *, #3541, .F. ) ;
#15602=DIRECTION ( 'NONE',  ( 1.000000000000000000, -2.270069654138870255E-15, -7.035747901516311190E-77 ) ) ;
#15622=CYLINDRICAL_SURFACE ( 'NONE', #6573, 7.000000000000000000 ) ;
#15624=CARTESIAN_POINT ( 'NONE',  ( -24.86147400983239919, -14.96352599016710094, 2.500000000000000000 ) ) ;
#15642=EDGE_LOOP ( 'NONE', ( #15375, #8376, #17225, #17584 ) ) ;
#15647=DIRECTION ( 'NONE',  ( 2.270069654138870255E-15, 1.000000000000000000, 7.035747901516317327E-77 ) ) ;
#15649=DIRECTION ( 'NONE',  ( -2.977235988022386522E-185, 9.605990953944227443E-124, 1.000000000000000000 ) ) ;
#15686=DIRECTION ( 'NONE',  ( 1.000000000000000000, 3.099353312215988811E-62, 0.000000000000000000 ) ) ;
#15757=VERTEX_POINT ( 'NONE', #4798 ) ;
#15771=EDGE_CURVE ( 'NONE', #3638, #12832, #6711, .T. ) ;
#15809=CARTESIAN_POINT ( 'NONE',  ( -27.00000000000000000, -20.00000000000000000, 5.000000000000000000 ) ) ;
#15856=DIRECTION ( 'NONE',  ( -0.6944962871189153120, 0.7194962871190101472, 0.000000000000000000 ) ) ;
#15861=ORIENTED_EDGE ( 'NONE', *, *, #17910, .F. ) ;
#15999=DIRECTION ( 'NONE',  ( -2.270069654138870255E-15, -1.000000000000000000, -7.035747901516317327E-77 ) ) ;
#16037=LINE ( 'NONE', #16691, #15196 ) ;
#16055=CARTESIAN_POINT ( 'NONE',  ( 6.500000000000000000, -1.630990338096509915E-14, 2.500000000000000000 ) ) ;
#16069=CARTESIAN_POINT ( 'NONE',  ( -4.514225866272930432, 4.676725866273559795, 5.000000000000000000 ) ) ;
#16072=VECTOR ( 'NONE', #18311, 1000.000000000000000 ) ;
#16154=DIRECTION ( 'NONE',  ( -3.099353312215989243E-62, 0.000000000000000000, 1.000000000000000000 ) ) ;
#16163=VERTEX_POINT ( 'NONE', #9539 ) ;
#16194=LINE ( 'NONE', #23426, #10621 ) ;
#16205=CARTESIAN_POINT ( 'NONE',  ( -1.262685242559879909E-14, -17.30000000000000071, 2.500000000000000000 ) ) ;
#16213=LINE ( 'NONE', #5634, #9528 ) ;
#16230=DIRECTION ( 'NONE',  ( 3.099353312215989243E-62, -9.554441540188157279E-93, -1.000000000000000000 ) ) ;
#16235=ADVANCED_FACE ( 'NONE', ( #1191 ), #2875, .T. ) ;
#16237=VERTEX_POINT ( 'NONE', #2983 ) ;
#16279=DIRECTION ( 'NONE',  ( 1.000000000000000000, -2.270069654138870255E-15, 3.099353312215988811E-62 ) ) ;
#16345=ADVANCED_FACE ( 'NONE', ( #13914 ), #13559, .F. ) ;
#16451=EDGE_CURVE ( 'NONE', #3638, #16709, #8455, .T. ) ;
#16477=EDGE_CURVE ( 'NONE', #4246, #15256, #5026, .T. ) ;
#16546=CARTESIAN_POINT ( 'NONE',  ( -16.50000000000000000, -20.00000000000000711, 2.500000000000000000 ) ) ;
#16576=ORIENTED_EDGE ( 'NONE', *, *, #3748, .F. ) ;
#16594=LINE ( 'NONE', #10823, #2891 ) ;
#16655=EDGE_CURVE ( 'NONE', #10873, #1296, #6581, .T. ) ;
#16687=CARTESIAN_POINT ( 'NONE',  ( -1.262685242559879909E-14, -17.30000000000000071, 5.000000000000000000 ) ) ;
#16691=CARTESIAN_POINT ( 'NONE',  ( -2.499999999999973799, 4.120723506284736299E-15, 2.500000000000000000 ) ) ;
#16706=DIRECTION ( 'NONE',  ( 1.000000000000000000, -1.991364888915564904E-60, -2.270069654138870255E-15 ) ) ;
#16708=VERTEX_POINT ( 'NONE', #4394 ) ;
#16709=VERTEX_POINT ( 'NONE', #2027 ) ;
#16729=DIRECTION ( 'NONE',  ( 0.7071067811865476838, -1.387778780781444689E-15, 0.7071067811865473507 ) ) ;
#16877=EDGE_LOOP ( 'NONE', ( #23013, #6648, #21637, #5764 ) ) ;
#16882=EDGE_CURVE ( 'NONE', #16163, #15133, #8085, .T. ) ;
#16922=CARTESIAN_POINT ( 'NONE',  ( 5.000000000000000000, -31.09999999999999787, 21.50000000000000000 ) ) ;
#16933=ORIENTED_EDGE ( 'NONE', *, *, #289, .T. ) ;
#17008=VERTEX_POINT ( 'NONE', #9014 ) ;
#17097=VECTOR ( 'NONE', #20632, 1000.000000000000000 ) ;
#17111=AXIS2_PLACEMENT_3D ( 'NONE', #17310, #15394, #11635 ) ;
#17116=VERTEX_POINT ( 'NONE', #8981 ) ;
#17139=MANIFOLD_SOLID_BREP ( 'Boss-Extrude1', #1085 ) ;
#17225=ORIENTED_EDGE ( 'NONE', *, *, #6545, .T. ) ;
#17238=EDGE_CURVE ( 'NONE', #20661, #10873, #14780, .T. ) ;
#17255=EDGE_CURVE ( 'NONE', #2924, #8909, #7359, .T. ) ;
#17281=LINE ( 'NONE', #17511, #8826 ) ;
#17310=CARTESIAN_POINT ( 'NONE',  ( -24.50000000000000000, -31.09999999999999787, 19.00000000000000000 ) ) ;
#17337=DIRECTION ( 'NONE',  ( -1.000000000000000000, 2.270069654138870255E-15, -3.099353312215988811E-62 ) ) ;
#17424=DIRECTION ( 'NONE',  ( 1.000000000000000000, -2.270069654138870255E-15, 3.099353312215988811E-62 ) ) ;
#17454=ORIENTED_EDGE ( 'NONE', *, *, #3854, .T. ) ;
#17455=ORIENTED_EDGE ( 'NONE', *, *, #2300, .F. ) ;
#17511=CARTESIAN_POINT ( 'NONE',  ( 2.500000000000026645, -7.535786464196452844E-15, 2.500000000000000000 ) ) ;
#17513=EDGE_CURVE ( 'NONE', #20176, #19233, #13445, .T. ) ;
#17517=CARTESIAN_POINT ( 'NONE',  ( -20.00000000000000000, -20.00000000000000000, 2.500000000000000000 ) ) ;
#17522=ORIENTED_EDGE ( 'NONE', *, *, #23317, .T. ) ;
#17530=DIRECTION ( 'NONE',  ( 0.000000000000000000, 0.000000000000000000, -1.000000000000000000 ) ) ;
#17566=CIRCLE ( 'NONE', #22855, 6.500000000000000888 ) ;
#17584=ORIENTED_EDGE ( 'NONE', *, *, #15771, .T. ) ;
#17594=CARTESIAN_POINT ( 'NONE',  ( 5.000000000000000000, -31.09999999999999787, 6.250000000000000000 ) ) ;
#17597=CIRCLE ( 'NONE', #2416, 2.500000000000000000 ) ;
#17621=EDGE_CURVE ( 'NONE', #10873, #11427, #9387, .T. ) ;
#17646=SHAPE_REPRESENTATION ( 'F3', ( #12739 ), #19550 ) ;
#17683=EDGE_CURVE ( 'NONE', #5287, #16237, #23270, .T. ) ;
#17717=ORIENTED_EDGE ( 'NONE', *, *, #16451, .T. ) ;
#17719=DIRECTION ( 'NONE',  ( -2.270069654138865127E-15, -1.000000000000000000, -4.574083617919690056E-30 ) ) ;
#17798=ORIENTED_EDGE ( 'NONE', *, *, #12845, .T. ) ;
#17853=FACE_OUTER_BOUND ( 'NONE', #3036, .T. ) ;
#17857=ADVANCED_FACE ( 'NONE', ( #810 ), #8084, .T. ) ;
#17893=VECTOR ( 'NONE', #5244, 1000.000000000000000 ) ;
#17897=DIRECTION ( 'NONE',  ( 3.099353312215989243E-62, 1.872670541876879671E-92, -1.000000000000000000 ) ) ;
#17910=EDGE_CURVE ( 'NONE', #8641, #20176, #9658, .T. ) ;
#17921=DIRECTION ( 'NONE',  ( -0.7071067811865475727, 1.387778780781445281E-15, 0.7071067811865475727 ) ) ;
#18081=ORIENTED_EDGE ( 'NONE', *, *, #19061, .T. ) ;
#18174=DIRECTION ( 'NONE',  ( 3.099353312215988811E-62, 0.000000000000000000, -1.000000000000000000 ) ) ;
#18197=AXIS2_PLACEMENT_3D ( 'NONE', #14314, #12544, #22244 ) ;
#18246=CARTESIAN_POINT ( 'NONE',  ( -1.262685242559879909E-14, -17.30000000000000071, 5.000000000000000000 ) ) ;
#18303=ORIENTED_EDGE ( 'NONE', *, *, #19845, .F. ) ;
#18311=DIRECTION ( 'NONE',  ( -2.270069654138870255E-15, -1.000000000000000000, -7.035747901516317327E-77 ) ) ;
#18322=AXIS2_PLACEMENT_3D ( 'NONE', #9903, #15349, #2169 ) ;
#18467=EDGE_CURVE ( 'NONE', #19614, #11427, #14090, .T. ) ;
#18494=CARTESIAN_POINT ( 'NONE',  ( -27.00000000000000000, -20.00000000000000000, 2.500000000000000000 ) ) ;
#18625=ORIENTED_EDGE ( 'NONE', *, *, #4874, .F. ) ;
#18654=DIRECTION ( 'NONE',  ( 1.000000000000000000, -2.270069654138870255E-15, 7.033657510914128686E-46 ) ) ;
#18666=DIRECTION ( 'NONE',  ( 2.270069654138865127E-15, 1.000000000000000000, 4.574083617919690056E-30 ) ) ;
#18689=CIRCLE ( 'NONE', #8445, 3.499999999999999556 ) ;
#18747=( NAMED_UNIT ( * ) SI_UNIT ( $, .STERADIAN. ) SOLID_ANGLE_UNIT ( ) );
#18783=CARTESIAN_POINT ( 'NONE',  ( -24.50000000000000000, -28.60000000000000142, 19.00000000000000000 ) ) ;
#18801=ORIENTED_EDGE ( 'NONE', *, *, #9969, .F. ) ;
#18804=ORIENTED_EDGE ( 'NONE', *, *, #15383, .F. ) ;
#18893=ORIENTED_EDGE ( 'NONE', *, *, #1252, .F. ) ;
#18950=ADVANCED_FACE ( 'NONE', ( #4803 ), #8721, .F. ) ;
#18951=VERTEX_POINT ( 'NONE', #20951 ) ;
#18962=VECTOR ( 'NONE', #19534, 999.9999999999998863 ) ;
#18969=AXIS2_PLACEMENT_3D ( 'NONE', #4796, #15602, #20943 ) ;
#18973=EDGE_LOOP ( 'NONE', ( #9551, #10132, #23281, #18804, #21117, #17455, #11167, #4854, #6469 ) ) ;
#19009=EDGE_CURVE ( 'NONE', #9430, #11527, #10414, .T. ) ;
#19058=CYLINDRICAL_SURFACE ( 'NONE', #9890, 2.500000000000000000 ) ;
#19061=EDGE_CURVE ( 'NONE', #19614, #19233, #6958, .T. ) ;
#19080=CIRCLE ( 'NONE', #22091, 6.500000000000000000 ) ;
#19087=PRODUCT_DEFINITION_FORMATION_WITH_SPECIFIED_SOURCE ( 'ANY', '', #4576, .NOT_KNOWN. ) ;
#19097=LINE ( 'NONE', #20634, #19612 ) ;
#19154=DIRECTION ( 'NONE',  ( -1.000000000000000000, 1.982541115402065307E-15, 0.000000000000000000 ) ) ;
#19176=FACE_OUTER_BOUND ( 'NONE', #22117, .T. ) ;
#19194=FACE_OUTER_BOUND ( 'NONE', #10958, .T. ) ;
#19195=PLANE ( 'NONE',  #2206 ) ;
#19233=VERTEX_POINT ( 'NONE', #19991 ) ;
#19238=EDGE_LOOP ( 'NONE', ( #14783, #89, #17717, #12429 ) ) ;
#19243=CIRCLE ( 'NONE', #23392, 2.500000000000000000 ) ;
#19257=DIRECTION ( 'NONE',  ( -1.000000000000000000, 2.270069654138870255E-15, -3.099353312215989243E-62 ) ) ;
#19265=CARTESIAN_POINT ( 'NONE',  ( -24.50000000000000000, -30.47499999999999787, 19.00000000000000000 ) ) ;
#19272=CARTESIAN_POINT ( 'NONE',  ( 6.500000000000000000, -1.630990338096509915E-14, 2.500000000000000000 ) ) ;
#19274=CIRCLE ( 'NONE', #9405, 2.500000000000000000 ) ;
#19283=CYLINDRICAL_SURFACE ( 'NONE', #14721, 2.500000000000000000 ) ;
#19295=DIRECTION ( 'NONE',  ( -3.099353312215989243E-62, 1.001855809244433740E-92, 1.000000000000000000 ) ) ;
#19338=CARTESIAN_POINT ( 'NONE',  ( 6.500000000000000000, -1.630990338096509915E-14, 5.000000000000000000 ) ) ;
#19339=ADVANCED_FACE ( 'NONE', ( #9678 ), #7998, .F. ) ;
#19414=EDGE_CURVE ( 'NONE', #11308, #11527, #8854, .T. ) ;
#19436=VECTOR ( 'NONE', #22960, 1000.000000000000000 ) ;
#19473=VERTEX_POINT ( 'NONE', #9787 ) ;
#19497=DIRECTION ( 'NONE',  ( -0.7071067811865475727, 1.387778780781445281E-15, 0.7071067811865475727 ) ) ;
#19530=ORIENTED_EDGE ( 'NONE', *, *, #15220, .F. ) ;
#19534=DIRECTION ( 'NONE',  ( 0.7194962871189621856, 0.6944962871189651610, 2.229973200609260484E-62 ) ) ;
#19550=( GEOMETRIC_REPRESENTATION_CONTEXT ( 3 ) GLOBAL_UNCERTAINTY_ASSIGNED_CONTEXT ( ( #1339 ) ) GLOBAL_UNIT_ASSIGNED_CONTEXT ( ( #22266, #13255, #18747 ) ) REPRESENTATION_CONTEXT ( 'NONE', 'WORKASPACE' ) );
#19551=LINE ( 'NONE', #10656, #1930 ) ;
#19612=VECTOR ( 'NONE', #15154, 1000.000000000000000 ) ;
#19614=VERTEX_POINT ( 'NONE', #4896 ) ;
#19637=CARTESIAN_POINT ( 'NONE',  ( 2.664535259100379799E-14, 6.659954201878760116E-16, 2.500000000000000000 ) ) ;
#19663=VECTOR ( 'NONE', #1912, 1000.000000000000000 ) ;
#19666=DIRECTION ( 'NONE',  ( -1.000000000000000000, 1.982541115402065307E-15, 0.000000000000000000 ) ) ;
#19731=ORIENTED_EDGE ( 'NONE', *, *, #13008, .F. ) ;
#19739=ADVANCED_FACE ( 'NONE', ( #5133 ), #12388, .T. ) ;
#19798=EDGE_CURVE ( 'NONE', #16708, #11308, #1550, .T. ) ;
#19803=CARTESIAN_POINT ( 'NONE',  ( 2.664535259100379799E-14, -1.554450629062440126E-15, 2.500000000000000000 ) ) ;
#19826=CIRCLE ( 'NONE', #21352, 6.499999999999998224 ) ;
#19827=DIRECTION ( 'NONE',  ( 2.270069654138870255E-15, 1.000000000000000000, 7.035747901516317327E-77 ) ) ;
#19845=EDGE_CURVE ( 'NONE', #8301, #4246, #8055, .T. ) ;
#19888=ORIENTED_EDGE ( 'NONE', *, *, #22449, .T. ) ;
#19955=CARTESIAN_POINT ( 'NONE',  ( -24.86147400983239919, -14.96352599016710094, 5.000000000000000000 ) ) ;
#19960=DIRECTION ( 'NONE',  ( 0.7071067811865476838, -1.387778780781444689E-15, 0.7071067811865473507 ) ) ;
#19991=CARTESIAN_POINT ( 'NONE',  ( -27.00000000000000000, -28.60000000000000142, 19.00000000000000000 ) ) ;
#20021=CARTESIAN_POINT ( 'NONE',  ( -2.500000000000012434, -17.29999999999999361, 2.500000000000000000 ) ) ;
#20046=ORIENTED_EDGE ( 'NONE', *, *, #20362, .T. ) ;
#20069=EDGE_LOOP ( 'NONE', ( #21449, #19888 ) ) ;
#20084=EDGE_CURVE ( 'NONE', #8301, #8641, #6862, .T. ) ;
#20087=VECTOR ( 'NONE', #13941, 1000.000000000000000 ) ;
#20103=ORIENTED_EDGE ( 'NONE', *, *, #2300, .T. ) ;
#20113=DIRECTION ( 'NONE',  ( -3.099353312215989243E-62, -1.872670541876879671E-92, 1.000000000000000000 ) ) ;
#20130=DIRECTION ( 'NONE',  ( 2.270069654138865127E-15, 1.000000000000000000, -4.574083617919690056E-30 ) ) ;
#20141=DIRECTION ( 'NONE',  ( 3.099353312215989243E-62, 0.000000000000000000, -1.000000000000000000 ) ) ;
#20154=EDGE_CURVE ( 'NONE', #20610, #12832, #19826, .T. ) ;
#20170=EDGE_CURVE ( 'NONE', #12606, #4246, #2199, .T. ) ;
#20176=VERTEX_POINT ( 'NONE', #12895 ) ;
#20264=DIRECTION ( 'NONE',  ( 0.8846153846154060085, -0.4663213712685030377, 0.000000000000000000 ) ) ;
#20276=ADVANCED_FACE ( 'NONE', ( #7209, #5421, #5766, #12679 ), #9222, .F. ) ;
#20307=CARTESIAN_POINT ( 'NONE',  ( -27.00000000000000000, -27.34999999999999787, 2.500000000000000000 ) ) ;
#20310=DIRECTION ( 'NONE',  ( 3.099353312215989243E-62, -9.554441540188157279E-93, -1.000000000000000000 ) ) ;
#20330=LINE ( 'NONE', #4059, #751 ) ;
#20360=EDGE_CURVE ( 'NONE', #12832, #6522, #17566, .T. ) ;
#20362=EDGE_CURVE ( 'NONE', #2081, #20661, #2800, .T. ) ;
#20373=EDGE_CURVE ( 'NONE', #16709, #20610, #22374, .T. ) ;
#20380=CIRCLE ( 'NONE', #7124, 2.500000000000000000 ) ;
#20384=DIRECTION ( 'NONE',  ( -1.000000000000000000, 2.775557561562891351E-15, 0.000000000000000000 ) ) ;
#20436=CARTESIAN_POINT ( 'NONE',  ( -26.26776695296636888, -31.09999999999999432, 20.76776695296636888 ) ) ;
#20464=DIRECTION ( 'NONE',  ( -1.000000000000000000, 2.270069654138870255E-15, 0.000000000000000000 ) ) ;
#20550=CARTESIAN_POINT ( 'NONE',  ( 5.000000000000000000, -23.36217782649100272, 5.000000000000000000 ) ) ;
#20610=VERTEX_POINT ( 'NONE', #7075 ) ;
#20628=VECTOR ( 'NONE', #17424, 1000.000000000000000 ) ;
#20630=ORIENTED_EDGE ( 'NONE', *, *, #22705, .F. ) ;
#20632=DIRECTION ( 'NONE',  ( 1.000000000000000000, -2.270069654138870255E-15, 3.099353312215988811E-62 ) ) ;
#20634=CARTESIAN_POINT ( 'NONE',  ( 5.000000000000000000, -31.09999999999999787, 2.500000000000000000 ) ) ;
#20657=CARTESIAN_POINT ( 'NONE',  ( -27.00000000000000000, -29.85000000000000142, 12.00000000000000000 ) ) ;
#20661=VERTEX_POINT ( 'NONE', #2909 ) ;
#20663=ORIENTED_EDGE ( 'NONE', *, *, #8474, .T. ) ;
#20707=DIRECTION ( 'NONE',  ( -3.099353312215989243E-62, -9.818186930595456717E-93, 1.000000000000000000 ) ) ;
#20722=CARTESIAN_POINT ( 'NONE',  ( 11.50000000000000000, -23.36217782649120167, 5.000000000000000000 ) ) ;
#20765=ORIENTED_EDGE ( 'NONE', *, *, #21632, .T. ) ;
#20789=VECTOR ( 'NONE', #22267, 1000.000000000000000 ) ;
#20834=CYLINDRICAL_SURFACE ( 'NONE', #15514, 2.500000000000001776 ) ;
#20884=CARTESIAN_POINT ( 'NONE',  ( 4.267766952966340455, -31.10000000000000142, 20.76776695296636532 ) ) ;
#20896=ORIENTED_EDGE ( 'NONE', *, *, #8939, .T. ) ;
#20915=ORIENTED_EDGE ( 'NONE', *, *, #19009, .T. ) ;
#20943=DIRECTION ( 'NONE',  ( 0.000000000000000000, -3.099353312215988811E-62, 1.000000000000000000 ) ) ;
#20950=ORIENTED_EDGE ( 'NONE', *, *, #4318, .F. ) ;
#20951=CARTESIAN_POINT ( 'NONE',  ( 5.000000000000000000, -27.34999999999999787, 5.000000000000000000 ) ) ;
#20959=AXIS2_PLACEMENT_3D ( 'NONE', #11144, #172, #14672 ) ;
#21000=VECTOR ( 'NONE', #13241, 1000.000000000000000 ) ;
#21012=AXIS2_PLACEMENT_3D ( 'NONE', #15316, #9998, #933 ) ;
#21036=CARTESIAN_POINT ( 'NONE',  ( 5.000000000000000000, -27.34999999999999787, 6.250000000000000000 ) ) ;
#21044=VECTOR ( 'NONE', #16279, 1000.000000000000000 ) ;
#21084=DIRECTION ( 'NONE',  ( 3.099353312215989243E-62, 1.872670541876879671E-92, -1.000000000000000000 ) ) ;
#21101=VERTEX_POINT ( 'NONE', #21275 ) ;
#21117=ORIENTED_EDGE ( 'NONE', *, *, #4301, .F. ) ;
#21150=DIRECTION ( 'NONE',  ( -0.7071067811865475727, 1.387778780781445281E-15, 0.7071067811865475727 ) ) ;
#21152=CARTESIAN_POINT ( 'NONE',  ( -1.262685242559879909E-14, -17.30000000000000071, 2.500000000000000000 ) ) ;
#21171=DIRECTION ( 'NONE',  ( -1.000000000000000000, 2.775557561562891351E-15, 0.000000000000000000 ) ) ;
#21175=PLANE ( 'NONE',  #18969 ) ;
#21177=DIRECTION ( 'NONE',  ( -3.099353312215988811E-62, 0.000000000000000000, 1.000000000000000000 ) ) ;
#21223=DIRECTION ( 'NONE',  ( -1.000000000000000000, 2.270069654138870255E-15, 0.000000000000000000 ) ) ;
#21275=CARTESIAN_POINT ( 'NONE',  ( 2.499999999999987566, -17.30000000000000782, 2.500000000000000000 ) ) ;
#21352=AXIS2_PLACEMENT_3D ( 'NONE', #18246, #20141, #20264 ) ;
#21353=CARTESIAN_POINT ( 'NONE',  ( -27.00000000000000000, -31.09999999999999787, 2.500000000000000000 ) ) ;
#21389=CARTESIAN_POINT ( 'NONE',  ( -24.50000000000000000, -28.60000000000000142, 19.00000000000000000 ) ) ;
#21415=LINE ( 'NONE', #2899, #20087 ) ;
#21427=EDGE_LOOP ( 'NONE', ( #16576, #17798, #13840, #22216 ) ) ;
#21449=ORIENTED_EDGE ( 'NONE', *, *, #10530, .T. ) ;
#21477=EDGE_LOOP ( 'NONE', ( #13046, #23353, #9447, #5579 ) ) ;
#21502=CARTESIAN_POINT ( 'NONE',  ( -27.00000000000000000, -20.00000000000000000, 5.000000000000000000 ) ) ;
#21627=LINE ( 'NONE', #14393, #19663 ) ;
#21632=EDGE_CURVE ( 'NONE', #6522, #18951, #188, .T. ) ;
#21637=ORIENTED_EDGE ( 'NONE', *, *, #10422, .T. ) ;
#21660=DIRECTION ( 'NONE',  ( -3.099353312215988811E-62, 1.001855809244433740E-92, 1.000000000000000000 ) ) ;
#21724=EDGE_CURVE ( 'NONE', #16163, #12545, #19097, .T. ) ;
#21848=ORIENTED_EDGE ( 'NONE', *, *, #8939, .F. ) ;
#21887=AXIS2_PLACEMENT_3D ( 'NONE', #19803, #2688, #15277 ) ;
#21922=DIRECTION ( 'NONE',  ( 3.099353312215989243E-62, 1.872670541876879671E-92, -1.000000000000000000 ) ) ;
#21954=CIRCLE ( 'NONE', #5285, 3.750000000000000000 ) ;
#21971=ORIENTED_EDGE ( 'NONE', *, *, #17621, .F. ) ;
#21989=ORIENTED_EDGE ( 'NONE', *, *, #8856, .T. ) ;
#21999=CARTESIAN_POINT ( 'NONE',  ( 4.267766952966340455, -28.60000000000000497, 20.76776695296636532 ) ) ;
#22002=CIRCLE ( 'NONE', #11797, 1.250000000000000222 ) ;
#22070=ORIENTED_EDGE ( 'NONE', *, *, #17621, .T. ) ;
#22082=VECTOR ( 'NONE', #4921, 1000.000000000000000 ) ;
#22091=AXIS2_PLACEMENT_3D ( 'NONE', #19637, #4916, #12183 ) ;
#22117=EDGE_LOOP ( 'NONE', ( #20896, #15443, #8027, #1839 ) ) ;
#22193=DIRECTION ( 'NONE',  ( -1.000000000000000000, 1.982541115402065307E-15, 0.000000000000000000 ) ) ;
#22216=ORIENTED_EDGE ( 'NONE', *, *, #10422, .F. ) ;
#22244=DIRECTION ( 'NONE',  ( -0.7071067811865475727, 1.387778780781445281E-15, 0.7071067811865475727 ) ) ;
#22266=( LENGTH_UNIT ( ) NAMED_UNIT ( * ) SI_UNIT ( .MILLI., .METRE. ) );
#22267=DIRECTION ( 'NONE',  ( -3.099353312215988811E-62, 0.000000000000000000, 1.000000000000000000 ) ) ;
#22374=LINE ( 'NONE', #4351, #12635 ) ;
#22426=CARTESIAN_POINT ( 'NONE',  ( -4.514225866272930432, 4.676725866273569565, 2.500000000000000000 ) ) ;
#22434=DIRECTION ( 'NONE',  ( -2.270069654138865127E-15, -1.000000000000000000, 4.574083617919690056E-30 ) ) ;
#22442=ORIENTED_EDGE ( 'NONE', *, *, #3571, .T. ) ;
#22449=EDGE_CURVE ( 'NONE', #21101, #5291, #19243, .T. ) ;
#22450=CIRCLE ( 'NONE', #1972, 6.500000000000000888 ) ;
#22510=AXIS2_PLACEMENT_3D ( 'NONE', #5942, #18666, #15086 ) ;
#22571=DIRECTION ( 'NONE',  ( -1.000000000000000000, 2.775557561562891351E-15, 0.000000000000000000 ) ) ;
#22600=AXIS2_PLACEMENT_3D ( 'NONE', #23370, #1302, #15686 ) ;
#22631=AXIS2_PLACEMENT_3D ( 'NONE', #8359, #12177, #2896 ) ;
#22668=ORIENTED_EDGE ( 'NONE', *, *, #18467, .T. ) ;
#22705=EDGE_CURVE ( 'NONE', #16708, #19614, #10177, .T. ) ;
#22708=LINE ( 'NONE', #6590, #8620 ) ;
#22727=ORIENTED_EDGE ( 'NONE', *, *, #17910, .T. ) ;
#22855=AXIS2_PLACEMENT_3D ( 'NONE', #20722, #11727, #6356 ) ;
#22889=FACE_OUTER_BOUND ( 'NONE', #6006, .T. ) ;
#22960=DIRECTION ( 'NONE',  ( -3.099353312215988811E-62, 0.000000000000000000, 1.000000000000000000 ) ) ;
#22972=DIRECTION ( 'NONE',  ( -1.000000000000000000, 2.270069654138870255E-15, -3.099353312215989243E-62 ) ) ;
#23013=ORIENTED_EDGE ( 'NONE', *, *, #12845, .F. ) ;
#23016=ORIENTED_EDGE ( 'NONE', *, *, #11909, .F. ) ;
#23028=PLANE ( 'NONE',  #22600 ) ;
#23034=DIRECTION ( 'NONE',  ( 0.000000000000000000, 0.000000000000000000, -1.000000000000000000 ) ) ;
#23036=ORIENTED_EDGE ( 'NONE', *, *, #17255, .T. ) ;
#23083=CYLINDRICAL_SURFACE ( 'NONE', #15486, 3.750000000000000000 ) ;
#23102=DIRECTION ( 'NONE',  ( 1.000000000000000000, -2.270069654138870255E-15, 7.403850011488566665E-46 ) ) ;
#23169=CIRCLE ( 'NONE', #15153, 2.500000000000000000 ) ;
#23200=VECTOR ( 'NONE', #15401, 1000.000000000000000 ) ;
#23226=ORIENTED_EDGE ( 'NONE', *, *, #14272, .T. ) ;
#23233=CARTESIAN_POINT ( 'NONE',  ( -1.262685242559879909E-14, -17.30000000000000071, 5.000000000000000000 ) ) ;
#23270=CIRCLE ( 'NONE', #11944, 3.499999999999999556 ) ;
#23281=ORIENTED_EDGE ( 'NONE', *, *, #11578, .F. ) ;
#23285=AXIS2_PLACEMENT_3D ( 'NONE', #12667, #7542, #5631 ) ;
#23317=EDGE_CURVE ( 'NONE', #1465, #11510, #13115, .T. ) ;
#23331=DIRECTION ( 'NONE',  ( -3.099353312215988811E-62, -9.818186930595456717E-93, 1.000000000000000000 ) ) ;
#23353=ORIENTED_EDGE ( 'NONE', *, *, #10309, .T. ) ;
#23370=CARTESIAN_POINT ( 'NONE',  ( -27.00000000000000000, -31.09999999999999787, 21.50000000000000000 ) ) ;
#23383=DIRECTION ( 'NONE',  ( -3.099353312215989243E-62, 2.689336210007789456E-77, 1.000000000000000000 ) ) ;
#23392=AXIS2_PLACEMENT_3D ( 'NONE', #9196, #20113, #4198 ) ;
#23411=AXIS2_PLACEMENT_3D ( 'NONE', #6335, #15473, #6444 ) ;
#23426=CARTESIAN_POINT ( 'NONE',  ( -27.00000000000000000, -31.09999999999999787, 6.250000000000000000 ) ) ;
#23436=DIRECTION ( 'NONE',  ( -3.099353312215989243E-62, -1.635250850668769823E-78, 1.000000000000000000 ) ) ;
#23457=DIRECTION ( 'NONE',  ( -2.270069654138870255E-15, -1.000000000000000000, -7.035747901516317327E-77 ) ) ;
#23515=COLOUR_RGB('Deep Blue', 0.09019608, 0.27058824, 0.51372549);
#23516=FILL_AREA_STYLE_COLOUR('',#23515);
#23517=FILL_AREA_STYLE('',(#23516));
#23518=SURFACE_STYLE_FILL_AREA(#23517);
#23519=SURFACE_SIDE_STYLE('',(#23518));
#23520=SURFACE_STYLE_USAGE(.BOTH.,#23519);
#23521=PRESENTATION_STYLE_ASSIGNMENT((#23520));
#23571=STYLED_ITEM('',(#23521),#17139);
#23572=MECHANICAL_DESIGN_GEOMETRIC_PRESENTATION_REPRESENTATION('',(#23571),#19550);
ENDSEC;
END-ISO-10303-21;
